ISO-10303-21;
HEADER;
/* Generated by software containing ST-Developer
 * from STEP Tools, Inc. (www.steptools.com) 
 */

FILE_DESCRIPTION(
/* description */ ('Spring compression tester'),
/* implementation_level */ '2;1');

FILE_NAME(
/* name */ 'Flat Washer - M6.step',
/* time_stamp */ '2026-10-28T03:24:11-07:00',
/* author */ (''),
/* organization */ (''),
/* preprocessor_version */ 'ST-DEVELOPER v20.2',
/* originating_system */ 'Autodesk Translation Framework v15.17.0.0',
/* authorisation */ '');

FILE_SCHEMA (('AUTOMOTIVE_DESIGN { 1 0 10303 214 3 1 1 }'));
ENDSEC;

DATA;
#10=MECHANICAL_DESIGN_GEOMETRIC_PRESENTATION_REPRESENTATION('',(#1177),#43521);
#1042=SHAPE_REPRESENTATION_RELATIONSHIP('SRR','None',#43859,#1102);
#1102=ADVANCED_BREP_SHAPE_REPRESENTATION('',(#1246),#43519);
#1177=STYLED_ITEM('',(#44209),#1246);
#1246=MANIFOLD_SOLID_BREP('Body1',#18620);
#1586=FACE_BOUND('',#4585,.T.);
#1587=FACE_BOUND('',#4587,.T.);
#2157=PLANE('',#21154);
#2158=PLANE('',#21155);
#3196=FACE_OUTER_BOUND('',#4582,.T.);
#3197=FACE_OUTER_BOUND('',#4583,.T.);
#3198=FACE_OUTER_BOUND('',#4584,.T.);
#3199=FACE_OUTER_BOUND('',#4586,.T.);
#4582=EDGE_LOOP('',(#17029,#17030,#17031,#17032));
#4583=EDGE_LOOP('',(#17033,#17034,#17035,#17036));
#4584=EDGE_LOOP('',(#17037));
#4585=EDGE_LOOP('',(#17038));
#4586=EDGE_LOOP('',(#17039));
#4587=EDGE_LOOP('',(#17040));
#6012=LINE('',#43292,#7444);
#6013=LINE('',#43298,#7445);
#7444=VECTOR('',#26334,0.32);
#7445=VECTOR('',#26341,0.6);
#8124=CIRCLE('',#21149,0.32);
#8125=CIRCLE('',#21150,0.32);
#8126=CIRCLE('',#21152,0.6);
#8127=CIRCLE('',#21153,0.6);
#9749=VERTEX_POINT('',#43289);
#9750=VERTEX_POINT('',#43291);
#9751=VERTEX_POINT('',#43295);
#9752=VERTEX_POINT('',#43297);
#12179=EDGE_CURVE('',#9749,#9749,#8124,.T.);
#12180=EDGE_CURVE('',#9749,#9750,#6012,.T.);
#12181=EDGE_CURVE('',#9750,#9750,#8125,.T.);
#12182=EDGE_CURVE('',#9751,#9751,#8126,.T.);
#12183=EDGE_CURVE('',#9751,#9752,#6013,.T.);
#12184=EDGE_CURVE('',#9752,#9752,#8127,.T.);
#17029=ORIENTED_EDGE('',*,*,#12179,.F.);
#17030=ORIENTED_EDGE('',*,*,#12180,.T.);
#17031=ORIENTED_EDGE('',*,*,#12181,.T.);
#17032=ORIENTED_EDGE('',*,*,#12180,.F.);
#17033=ORIENTED_EDGE('',*,*,#12182,.F.);
#17034=ORIENTED_EDGE('',*,*,#12183,.T.);
#17035=ORIENTED_EDGE('',*,*,#12184,.T.);
#17036=ORIENTED_EDGE('',*,*,#12183,.F.);
#17037=ORIENTED_EDGE('',*,*,#12182,.T.);
#17038=ORIENTED_EDGE('',*,*,#12179,.T.);
#17039=ORIENTED_EDGE('',*,*,#12184,.F.);
#17040=ORIENTED_EDGE('',*,*,#12181,.F.);
#17490=CYLINDRICAL_SURFACE('',#21148,0.32);
#17491=CYLINDRICAL_SURFACE('',#21151,0.6);
#18520=ADVANCED_FACE('',(#3196),#17490,.F.);
#18521=ADVANCED_FACE('',(#3197),#17491,.T.);
#18522=ADVANCED_FACE('',(#3198,#1586),#2157,.T.);
#18523=ADVANCED_FACE('',(#3199,#1587),#2158,.F.);
#18620=CLOSED_SHELL('',(#18520,#18521,#18522,#18523));
#21147=AXIS2_PLACEMENT_3D('',#43287,#26328,#26329);
#21148=AXIS2_PLACEMENT_3D('',#43288,#26330,#26331);
#21149=AXIS2_PLACEMENT_3D('',#43290,#26332,#26333);
#21150=AXIS2_PLACEMENT_3D('',#43293,#26335,#26336);
#21151=AXIS2_PLACEMENT_3D('',#43294,#26337,#26338);
#21152=AXIS2_PLACEMENT_3D('',#43296,#26339,#26340);
#21153=AXIS2_PLACEMENT_3D('',#43299,#26342,#26343);
#21154=AXIS2_PLACEMENT_3D('',#43300,#26344,#26345);
#21155=AXIS2_PLACEMENT_3D('',#43301,#26346,#26347);
#26328=DIRECTION('axis',(0.,0.,1.));
#26329=DIRECTION('refdir',(1.,0.,0.));
#26330=DIRECTION('center_axis',(0.,1.,0.));
#26331=DIRECTION('ref_axis',(1.,0.,0.));
#26332=DIRECTION('center_axis',(0.,-1.,0.));
#26333=DIRECTION('ref_axis',(1.,0.,0.));
#26334=DIRECTION('',(0.,-1.,0.));
#26335=DIRECTION('center_axis',(0.,-1.,0.));
#26336=DIRECTION('ref_axis',(1.,0.,0.));
#26337=DIRECTION('center_axis',(0.,1.,0.));
#26338=DIRECTION('ref_axis',(1.,0.,0.));
#26339=DIRECTION('center_axis',(0.,1.,0.));
#26340=DIRECTION('ref_axis',(1.,0.,0.));
#26341=DIRECTION('',(0.,-1.,0.));
#26342=DIRECTION('center_axis',(0.,1.,0.));
#26343=DIRECTION('ref_axis',(1.,0.,0.));
#26344=DIRECTION('center_axis',(0.,1.,0.));
#26345=DIRECTION('ref_axis',(1.,0.,0.));
#26346=DIRECTION('center_axis',(0.,1.,0.));
#26347=DIRECTION('ref_axis',(1.,0.,0.));
#43287=CARTESIAN_POINT('',(0.,0.,0.));
#43288=CARTESIAN_POINT('Origin',(0.,0.,0.));
#43289=CARTESIAN_POINT('',(-0.32,0.16,3.91886975727153E-17));
#43290=CARTESIAN_POINT('Origin',(0.,0.16,0.));
#43291=CARTESIAN_POINT('',(-0.32,0.,3.91886975727153E-17));
#43292=CARTESIAN_POINT('',(-0.32,0.,3.91886975727153E-17));
#43293=CARTESIAN_POINT('Origin',(0.,0.,0.));
#43294=CARTESIAN_POINT('Origin',(0.,0.,0.));
#43295=CARTESIAN_POINT('',(-0.6,0.16,7.34788079488412E-17));
#43296=CARTESIAN_POINT('Origin',(0.,0.16,0.));
#43297=CARTESIAN_POINT('',(-0.6,0.,7.34788079488412E-17));
#43298=CARTESIAN_POINT('',(-0.6,0.,7.34788079488412E-17));
#43299=CARTESIAN_POINT('Origin',(0.,0.,0.));
#43300=CARTESIAN_POINT('Origin',(0.,0.16,0.));
#43301=CARTESIAN_POINT('Origin',(0.,0.,0.));
#43451=UNCERTAINTY_MEASURE_WITH_UNIT(LENGTH_MEASURE(0.001),#43522,
'DISTANCE_ACCURACY_VALUE',
'Maximum model space distance between geometric entities at asserted c
onnectivities');
#43453=UNCERTAINTY_MEASURE_WITH_UNIT(LENGTH_MEASURE(0.001),#43522,
'DISTANCE_ACCURACY_VALUE',
'Maximum model space distance between geometric entities at asserted c
onnectivities');
#43519=(
GEOMETRIC_REPRESENTATION_CONTEXT(3)
GLOBAL_UNCERTAINTY_ASSIGNED_CONTEXT((#43451))
GLOBAL_UNIT_ASSIGNED_CONTEXT((#43522,#43524,#43525))
REPRESENTATION_CONTEXT('','3D')
);
#43521=(
GEOMETRIC_REPRESENTATION_CONTEXT(3)
GLOBAL_UNCERTAINTY_ASSIGNED_CONTEXT((#43453))
GLOBAL_UNIT_ASSIGNED_CONTEXT((#43522,#43524,#43525))
REPRESENTATION_CONTEXT('','3D')
);
#43522=(
LENGTH_UNIT()
NAMED_UNIT(*)
SI_UNIT(.CENTI.,.METRE.)
);
#43524=(
NAMED_UNIT(*)
PLANE_ANGLE_UNIT()
SI_UNIT($,.RADIAN.)
);
#43525=(
NAMED_UNIT(*)
SI_UNIT($,.STERADIAN.)
SOLID_ANGLE_UNIT()
);
#43591=SHAPE_DEFINITION_REPRESENTATION(#43778,#43859);
#43778=PRODUCT_DEFINITION_SHAPE('',$,#43927);
#43859=SHAPE_REPRESENTATION('',(#21147),#43519);
#43861=PRODUCT_DEFINITION_CONTEXT('part definition',#44064,'design');
#43927=PRODUCT_DEFINITION('Flat Washer - M6','Flat Washer - M6',#43994,
#43861);
#43994=PRODUCT_DEFINITION_FORMATION('',$,#44131);
#44064=APPLICATION_CONTEXT(
'Core Data for Automotive Mechanical Design Process');
#44065=PRODUCT_CONTEXT('part definition',#44064,'mechanical');
#44131=PRODUCT('Flat Washer - M6','Flat Washer - M6','Flat Washer - M6',
(#44065));
#44203=COLOUR_RGB('Black',0.12,0.14,0.17);
#44204=FILL_AREA_STYLE_COLOUR('',#44203);
#44205=FILL_AREA_STYLE('',(#44204));
#44206=SURFACE_STYLE_FILL_AREA(#44205);
#44207=SURFACE_SIDE_STYLE('',(#44206));
#44208=SURFACE_STYLE_USAGE(.BOTH.,#44207);
#44209=PRESENTATION_STYLE_ASSIGNMENT((#44208));
ENDSEC;
END-ISO-10303-21;
